ISO-10303-21;
HEADER;
/* Generated by software containing ST-Developer
 * from STEP Tools, Inc. (www.steptools.com) 
 */

FILE_DESCRIPTION(
/* description */ ('Shaft runout checking stand'),
/* implementation_level */ '2;1');

FILE_NAME(
/* name */ 'Inner race spacer (5).step',
/* time_stamp */ '2026-11-02T21:12:33-08:00',
/* author */ (''),
/* organization */ (''),
/* preprocessor_version */ 'ST-DEVELOPER v20.2',
/* originating_system */ 'Autodesk Translation Framework v15.17.0.0',
/* authorisation */ '');

FILE_SCHEMA (('AUTOMOTIVE_DESIGN { 1 0 10303 214 3 1 1 }'));
ENDSEC;

DATA;
#10=MECHANICAL_DESIGN_GEOMETRIC_PRESENTATION_REPRESENTATION('',(#480),#11748);
#394=SHAPE_REPRESENTATION_RELATIONSHIP('SRR','None',#11943,#437);
#437=ADVANCED_BREP_SHAPE_REPRESENTATION('',(#530),#11719);
#480=STYLED_ITEM('',(#12170),#530);
#530=MANIFOLD_SOLID_BREP('Body1',#6224);
#624=FACE_BOUND('',#1652,.T.);
#625=FACE_BOUND('',#1654,.T.);
#773=CIRCLE('',#7038,0.505);
#774=CIRCLE('',#7039,0.505);
#775=CIRCLE('',#7041,0.7);
#776=CIRCLE('',#7042,0.7);
#985=CYLINDRICAL_SURFACE('',#7037,0.505);
#986=CYLINDRICAL_SURFACE('',#7040,0.7);
#1219=FACE_OUTER_BOUND('',#1649,.T.);
#1220=FACE_OUTER_BOUND('',#1650,.T.);
#1221=FACE_OUTER_BOUND('',#1651,.T.);
#1222=FACE_OUTER_BOUND('',#1653,.T.);
#1649=EDGE_LOOP('',(#4914,#4915,#4916,#4917));
#1650=EDGE_LOOP('',(#4918,#4919,#4920,#4921));
#1651=EDGE_LOOP('',(#4922));
#1652=EDGE_LOOP('',(#4923));
#1653=EDGE_LOOP('',(#4924));
#1654=EDGE_LOOP('',(#4925));
#2196=LINE('',#10367,#2663);
#2197=LINE('',#10373,#2664);
#2663=VECTOR('',#8413,0.505);
#2664=VECTOR('',#8420,0.7);
#3093=VERTEX_POINT('',#10364);
#3094=VERTEX_POINT('',#10366);
#3095=VERTEX_POINT('',#10370);
#3096=VERTEX_POINT('',#10372);
#3743=EDGE_CURVE('',#3093,#3093,#773,.T.);
#3744=EDGE_CURVE('',#3093,#3094,#2196,.T.);
#3745=EDGE_CURVE('',#3094,#3094,#774,.T.);
#3746=EDGE_CURVE('',#3095,#3095,#775,.T.);
#3747=EDGE_CURVE('',#3095,#3096,#2197,.T.);
#3748=EDGE_CURVE('',#3096,#3096,#776,.T.);
#4914=ORIENTED_EDGE('',*,*,#3743,.F.);
#4915=ORIENTED_EDGE('',*,*,#3744,.T.);
#4916=ORIENTED_EDGE('',*,*,#3745,.T.);
#4917=ORIENTED_EDGE('',*,*,#3744,.F.);
#4918=ORIENTED_EDGE('',*,*,#3746,.F.);
#4919=ORIENTED_EDGE('',*,*,#3747,.T.);
#4920=ORIENTED_EDGE('',*,*,#3748,.T.);
#4921=ORIENTED_EDGE('',*,*,#3747,.F.);
#4922=ORIENTED_EDGE('',*,*,#3746,.T.);
#4923=ORIENTED_EDGE('',*,*,#3743,.T.);
#4924=ORIENTED_EDGE('',*,*,#3748,.F.);
#4925=ORIENTED_EDGE('',*,*,#3745,.F.);
#5734=PLANE('',#7043);
#5735=PLANE('',#7044);
#6019=ADVANCED_FACE('',(#1219),#985,.F.);
#6020=ADVANCED_FACE('',(#1220),#986,.T.);
#6021=ADVANCED_FACE('',(#1221,#624),#5734,.T.);
#6022=ADVANCED_FACE('',(#1222,#625),#5735,.F.);
#6224=CLOSED_SHELL('',(#6019,#6020,#6021,#6022));
#7036=AXIS2_PLACEMENT_3D('',#10362,#8407,#8408);
#7037=AXIS2_PLACEMENT_3D('',#10363,#8409,#8410);
#7038=AXIS2_PLACEMENT_3D('',#10365,#8411,#8412);
#7039=AXIS2_PLACEMENT_3D('',#10368,#8414,#8415);
#7040=AXIS2_PLACEMENT_3D('',#10369,#8416,#8417);
#7041=AXIS2_PLACEMENT_3D('',#10371,#8418,#8419);
#7042=AXIS2_PLACEMENT_3D('',#10374,#8421,#8422);
#7043=AXIS2_PLACEMENT_3D('',#10375,#8423,#8424);
#7044=AXIS2_PLACEMENT_3D('',#10376,#8425,#8426);
#8407=DIRECTION('axis',(0.,0.,1.));
#8408=DIRECTION('refdir',(1.,0.,0.));
#8409=DIRECTION('center_axis',(0.,1.,0.));
#8410=DIRECTION('ref_axis',(1.,0.,0.));
#8411=DIRECTION('center_axis',(0.,-1.,0.));
#8412=DIRECTION('ref_axis',(1.,0.,0.));
#8413=DIRECTION('',(0.,-1.,0.));
#8414=DIRECTION('center_axis',(0.,-1.,0.));
#8415=DIRECTION('ref_axis',(1.,0.,0.));
#8416=DIRECTION('center_axis',(0.,1.,0.));
#8417=DIRECTION('ref_axis',(1.,0.,0.));
#8418=DIRECTION('center_axis',(0.,1.,0.));
#8419=DIRECTION('ref_axis',(1.,0.,0.));
#8420=DIRECTION('',(0.,-1.,0.));
#8421=DIRECTION('center_axis',(0.,1.,0.));
#8422=DIRECTION('ref_axis',(1.,0.,0.));
#8423=DIRECTION('center_axis',(0.,1.,0.));
#8424=DIRECTION('ref_axis',(1.,0.,0.));
#8425=DIRECTION('center_axis',(0.,1.,0.));
#8426=DIRECTION('ref_axis',(1.,0.,0.));
#10362=CARTESIAN_POINT('',(0.,0.,0.));
#10363=CARTESIAN_POINT('Origin',(-2.,10.45,5.));
#10364=CARTESIAN_POINT('',(-2.505,10.8,5.));
#10365=CARTESIAN_POINT('Origin',(-2.,10.8,5.));
#10366=CARTESIAN_POINT('',(-2.505,10.45,5.));
#10367=CARTESIAN_POINT('',(-2.505,10.45,5.));
#10368=CARTESIAN_POINT('Origin',(-2.,10.45,5.));
#10369=CARTESIAN_POINT('Origin',(-2.,10.45,5.));
#10370=CARTESIAN_POINT('',(-2.7,10.8,5.));
#10371=CARTESIAN_POINT('Origin',(-2.,10.8,5.));
#10372=CARTESIAN_POINT('',(-2.7,10.45,5.));
#10373=CARTESIAN_POINT('',(-2.7,10.45,5.));
#10374=CARTESIAN_POINT('Origin',(-2.,10.45,5.));
#10375=CARTESIAN_POINT('Origin',(-2.,10.8,5.));
#10376=CARTESIAN_POINT('Origin',(-2.,10.45,5.));
#11670=UNCERTAINTY_MEASURE_WITH_UNIT(LENGTH_MEASURE(0.001),#11749,
'DISTANCE_ACCURACY_VALUE',
'Maximum model space distance between geometric entities at asserted c
onnectivities');
#11699=UNCERTAINTY_MEASURE_WITH_UNIT(LENGTH_MEASURE(0.001),#11749,
'DISTANCE_ACCURACY_VALUE',
'Maximum model space distance between geometric entities at asserted c
onnectivities');
#11719=(
GEOMETRIC_REPRESENTATION_CONTEXT(3)
GLOBAL_UNCERTAINTY_ASSIGNED_CONTEXT((#11670))
GLOBAL_UNIT_ASSIGNED_CONTEXT((#11749,#11751,#11752))
REPRESENTATION_CONTEXT('','3D')
);
#11748=(
GEOMETRIC_REPRESENTATION_CONTEXT(3)
GLOBAL_UNCERTAINTY_ASSIGNED_CONTEXT((#11699))
GLOBAL_UNIT_ASSIGNED_CONTEXT((#11749,#11751,#11752))
REPRESENTATION_CONTEXT('','3D')
);
#11749=(
LENGTH_UNIT()
NAMED_UNIT(*)
SI_UNIT(.CENTI.,.METRE.)
);
#11751=(
NAMED_UNIT(*)
PLANE_ANGLE_UNIT()
SI_UNIT($,.RADIAN.)
);
#11752=(
NAMED_UNIT(*)
SI_UNIT($,.STERADIAN.)
SOLID_ANGLE_UNIT()
);
#11772=SHAPE_DEFINITION_REPRESENTATION(#11820,#11943);
#11820=PRODUCT_DEFINITION_SHAPE('',$,#11992);
#11943=SHAPE_REPRESENTATION('',(#7036),#11719);
#11972=PRODUCT_DEFINITION_CONTEXT('part definition',#12118,'design');
#11992=PRODUCT_DEFINITION('Inner race spacer_3','Inner race spacer (5)',
#12040,#11972);
#12040=PRODUCT_DEFINITION_FORMATION('',$,#12139);
#12118=APPLICATION_CONTEXT(
'Core Data for Automotive Mechanical Design Process');
#12119=PRODUCT_CONTEXT('part definition',#12118,'mechanical');
#12139=PRODUCT('Inner race spacer_3','Inner race spacer (5)',
'Inner race spacer',(#12119));
#12170=PRESENTATION_STYLE_ASSIGNMENT((#12175));
#12175=SURFACE_STYLE_USAGE(.BOTH.,#12180);
#12180=SURFACE_SIDE_STYLE('',(#12185));
#12185=SURFACE_STYLE_FILL_AREA(#12190);
#12190=FILL_AREA_STYLE('CAD Library Painted - Steel gray',(#12195));
#12195=FILL_AREA_STYLE_COLOUR('CAD Library Painted - Steel gray',#12200);
#12200=COLOUR_RGB('CAD Library Painted - Steel gray',0.592156862745098,
0.631372549019608,0.67843137254902);
ENDSEC;
END-ISO-10303-21;
